ISO-10303-21;
HEADER;
/* Generated by software containing ST-Developer
 * from STEP Tools, Inc. (www.steptools.com) 
 */

FILE_DESCRIPTION(
/* description */ (''),
/* implementation_level */ '2;1');

FILE_NAME(
/* name */ 'PO4.step',
/* time_stamp */ '2026-10-06T10:18:54-07:00',
/* author */ (''),
/* organization */ (''),
/* preprocessor_version */ 'ST-DEVELOPER v20.2',
/* originating_system */ 'Autodesk Translation Framework v15.15.0.0',
/* authorisation */ '');

FILE_SCHEMA (('AUTOMOTIVE_DESIGN { 1 0 10303 214 3 1 1 }'));
ENDSEC;

DATA;
#10=MECHANICAL_DESIGN_GEOMETRIC_PRESENTATION_REPRESENTATION('',(#88),#8445);
#70=SHAPE_REPRESENTATION_RELATIONSHIP('SRR','None',#8491,#79);
#79=ADVANCED_BREP_SHAPE_REPRESENTATION('',(#97),#8443);
#88=STYLED_ITEM('',(#8537),#97);
#97=MANIFOLD_SOLID_BREP('Body1',#4009);
#162=CYLINDRICAL_SURFACE('',#4458,9.5);
#163=CYLINDRICAL_SURFACE('',#4466,9.5);
#164=CYLINDRICAL_SURFACE('',#4470,6.5);
#165=CYLINDRICAL_SURFACE('',#4475,6.50000009685755);
#166=CYLINDRICAL_SURFACE('',#4478,4.75);
#167=CYLINDRICAL_SURFACE('',#4480,6.5);
#168=CYLINDRICAL_SURFACE('',#4484,8.);
#205=TOROIDAL_SURFACE('',#4453,8.,1.5);
#206=TOROIDAL_SURFACE('',#4462,12.0000001788139,4.1);
#364=FACE_BOUND('',#1003,.T.);
#365=FACE_BOUND('',#1006,.T.);
#366=FACE_BOUND('',#1012,.T.);
#367=FACE_BOUND('',#1015,.T.);
#368=FACE_BOUND('',#1017,.T.);
#506=CIRCLE('',#4454,8.);
#507=CIRCLE('',#4455,1.5);
#508=CIRCLE('',#4456,9.5);
#509=CIRCLE('',#4457,9.5);
#510=CIRCLE('',#4459,9.5);
#511=CIRCLE('',#4460,9.5);
#512=CIRCLE('',#4463,9.5);
#513=CIRCLE('',#4464,9.5);
#514=CIRCLE('',#4465,4.1);
#515=CIRCLE('',#4467,9.5);
#516=CIRCLE('',#4469,6.5);
#517=CIRCLE('',#4471,6.5);
#518=CIRCLE('',#4473,6.50000009685755);
#519=CIRCLE('',#4474,4.75);
#520=CIRCLE('',#4476,6.50000009685755);
#521=CIRCLE('',#4479,4.75);
#522=CIRCLE('',#4481,6.5);
#523=CIRCLE('',#4482,6.5);
#524=CIRCLE('',#4485,8.);
#525=CIRCLE('',#4486,8.);
#735=FACE_OUTER_BOUND('',#997,.T.);
#736=FACE_OUTER_BOUND('',#998,.T.);
#737=FACE_OUTER_BOUND('',#999,.T.);
#738=FACE_OUTER_BOUND('',#1000,.T.);
#739=FACE_OUTER_BOUND('',#1001,.T.);
#740=FACE_OUTER_BOUND('',#1002,.T.);
#741=FACE_OUTER_BOUND('',#1004,.T.);
#742=FACE_OUTER_BOUND('',#1005,.T.);
#743=FACE_OUTER_BOUND('',#1007,.T.);
#744=FACE_OUTER_BOUND('',#1008,.T.);
#745=FACE_OUTER_BOUND('',#1009,.T.);
#746=FACE_OUTER_BOUND('',#1010,.T.);
#747=FACE_OUTER_BOUND('',#1011,.T.);
#748=FACE_OUTER_BOUND('',#1013,.T.);
#749=FACE_OUTER_BOUND('',#1014,.T.);
#750=FACE_OUTER_BOUND('',#1016,.T.);
#997=EDGE_LOOP('',(#3551,#3552,#3553,#3554,#3555));
#998=EDGE_LOOP('',(#3556,#3557,#3558,#3559,#3560,#3561));
#999=EDGE_LOOP('',(#3562));
#1000=EDGE_LOOP('',(#3563,#3564,#3565,#3566,#3567,#3568));
#1001=EDGE_LOOP('',(#3569,#3570,#3571,#3572,#3573));
#1002=EDGE_LOOP('',(#3574));
#1003=EDGE_LOOP('',(#3575));
#1004=EDGE_LOOP('',(#3576,#3577,#3578,#3579));
#1005=EDGE_LOOP('',(#3580));
#1006=EDGE_LOOP('',(#3581));
#1007=EDGE_LOOP('',(#3582,#3583,#3584,#3585));
#1008=EDGE_LOOP('',(#3586));
#1009=EDGE_LOOP('',(#3587,#3588,#3589,#3590));
#1010=EDGE_LOOP('',(#3591,#3592,#3593,#3594));
#1011=EDGE_LOOP('',(#3595));
#1012=EDGE_LOOP('',(#3596));
#1013=EDGE_LOOP('',(#3597,#3598,#3599,#3600));
#1014=EDGE_LOOP('',(#3601));
#1015=EDGE_LOOP('',(#3602));
#1016=EDGE_LOOP('',(#3603));
#1017=EDGE_LOOP('',(#3604));
#1286=LINE('',#8309,#1575);
#1287=LINE('',#8322,#1576);
#1288=LINE('',#8329,#1577);
#1289=LINE('',#8339,#1578);
#1290=LINE('',#8343,#1579);
#1291=LINE('',#8349,#1580);
#1292=LINE('',#8356,#1581);
#1575=VECTOR('',#5467,9.5);
#1576=VECTOR('',#5484,9.5);
#1577=VECTOR('',#5493,6.5);
#1578=VECTOR('',#5506,6.50000009685755);
#1579=VECTOR('',#5511,4.75);
#1580=VECTOR('',#5518,6.5);
#1581=VECTOR('',#5527,8.);
#1930=VERTEX_POINT('',#8300);
#1931=VERTEX_POINT('',#8302);
#1932=VERTEX_POINT('',#8304);
#1933=VERTEX_POINT('',#8308);
#1934=VERTEX_POINT('',#8310);
#1935=VERTEX_POINT('',#8315);
#1936=VERTEX_POINT('',#8316);
#1937=VERTEX_POINT('',#8321);
#1938=VERTEX_POINT('',#8325);
#1939=VERTEX_POINT('',#8328);
#1940=VERTEX_POINT('',#8332);
#1941=VERTEX_POINT('',#8334);
#1942=VERTEX_POINT('',#8337);
#1943=VERTEX_POINT('',#8342);
#1944=VERTEX_POINT('',#8346);
#1945=VERTEX_POINT('',#8348);
#1946=VERTEX_POINT('',#8353);
#1947=VERTEX_POINT('',#8355);
#2476=EDGE_CURVE('',#1930,#1930,#506,.T.);
#2477=EDGE_CURVE('',#1930,#1931,#507,.T.);
#2478=EDGE_CURVE('',#1931,#1932,#508,.T.);
#2479=EDGE_CURVE('',#1932,#1931,#509,.T.);
#2480=EDGE_CURVE('',#1932,#1933,#1286,.T.);
#2481=EDGE_CURVE('',#1933,#1934,#510,.T.);
#2482=EDGE_CURVE('',#1934,#1933,#511,.T.);
#2483=EDGE_CURVE('',#1935,#1936,#512,.T.);
#2484=EDGE_CURVE('',#1936,#1935,#513,.T.);
#2485=EDGE_CURVE('',#1936,#1934,#514,.T.);
#2486=EDGE_CURVE('',#1935,#1937,#1287,.T.);
#2487=EDGE_CURVE('',#1937,#1937,#515,.T.);
#2488=EDGE_CURVE('',#1938,#1938,#516,.T.);
#2489=EDGE_CURVE('',#1938,#1939,#1288,.T.);
#2490=EDGE_CURVE('',#1939,#1939,#517,.T.);
#2491=EDGE_CURVE('',#1940,#1940,#518,.T.);
#2492=EDGE_CURVE('',#1941,#1941,#519,.T.);
#2493=EDGE_CURVE('',#1942,#1942,#520,.T.);
#2494=EDGE_CURVE('',#1942,#1940,#1289,.T.);
#2495=EDGE_CURVE('',#1941,#1943,#1290,.T.);
#2496=EDGE_CURVE('',#1943,#1943,#521,.T.);
#2497=EDGE_CURVE('',#1944,#1944,#522,.T.);
#2498=EDGE_CURVE('',#1944,#1945,#1291,.T.);
#2499=EDGE_CURVE('',#1945,#1945,#523,.T.);
#2500=EDGE_CURVE('',#1946,#1946,#524,.T.);
#2501=EDGE_CURVE('',#1946,#1947,#1292,.T.);
#2502=EDGE_CURVE('',#1947,#1947,#525,.T.);
#3551=ORIENTED_EDGE('',*,*,#2476,.T.);
#3552=ORIENTED_EDGE('',*,*,#2477,.T.);
#3553=ORIENTED_EDGE('',*,*,#2478,.T.);
#3554=ORIENTED_EDGE('',*,*,#2479,.T.);
#3555=ORIENTED_EDGE('',*,*,#2477,.F.);
#3556=ORIENTED_EDGE('',*,*,#2479,.F.);
#3557=ORIENTED_EDGE('',*,*,#2480,.T.);
#3558=ORIENTED_EDGE('',*,*,#2481,.T.);
#3559=ORIENTED_EDGE('',*,*,#2482,.T.);
#3560=ORIENTED_EDGE('',*,*,#2480,.F.);
#3561=ORIENTED_EDGE('',*,*,#2478,.F.);
#3562=ORIENTED_EDGE('',*,*,#2476,.F.);
#3563=ORIENTED_EDGE('',*,*,#2483,.F.);
#3564=ORIENTED_EDGE('',*,*,#2484,.F.);
#3565=ORIENTED_EDGE('',*,*,#2485,.T.);
#3566=ORIENTED_EDGE('',*,*,#2481,.F.);
#3567=ORIENTED_EDGE('',*,*,#2482,.F.);
#3568=ORIENTED_EDGE('',*,*,#2485,.F.);
#3569=ORIENTED_EDGE('',*,*,#2483,.T.);
#3570=ORIENTED_EDGE('',*,*,#2484,.T.);
#3571=ORIENTED_EDGE('',*,*,#2486,.T.);
#3572=ORIENTED_EDGE('',*,*,#2487,.T.);
#3573=ORIENTED_EDGE('',*,*,#2486,.F.);
#3574=ORIENTED_EDGE('',*,*,#2487,.F.);
#3575=ORIENTED_EDGE('',*,*,#2488,.T.);
#3576=ORIENTED_EDGE('',*,*,#2488,.F.);
#3577=ORIENTED_EDGE('',*,*,#2489,.T.);
#3578=ORIENTED_EDGE('',*,*,#2490,.F.);
#3579=ORIENTED_EDGE('',*,*,#2489,.F.);
#3580=ORIENTED_EDGE('',*,*,#2491,.F.);
#3581=ORIENTED_EDGE('',*,*,#2492,.T.);
#3582=ORIENTED_EDGE('',*,*,#2493,.F.);
#3583=ORIENTED_EDGE('',*,*,#2494,.T.);
#3584=ORIENTED_EDGE('',*,*,#2491,.T.);
#3585=ORIENTED_EDGE('',*,*,#2494,.F.);
#3586=ORIENTED_EDGE('',*,*,#2493,.T.);
#3587=ORIENTED_EDGE('',*,*,#2492,.F.);
#3588=ORIENTED_EDGE('',*,*,#2495,.T.);
#3589=ORIENTED_EDGE('',*,*,#2496,.F.);
#3590=ORIENTED_EDGE('',*,*,#2495,.F.);
#3591=ORIENTED_EDGE('',*,*,#2497,.F.);
#3592=ORIENTED_EDGE('',*,*,#2498,.T.);
#3593=ORIENTED_EDGE('',*,*,#2499,.F.);
#3594=ORIENTED_EDGE('',*,*,#2498,.F.);
#3595=ORIENTED_EDGE('',*,*,#2497,.T.);
#3596=ORIENTED_EDGE('',*,*,#2496,.T.);
#3597=ORIENTED_EDGE('',*,*,#2500,.F.);
#3598=ORIENTED_EDGE('',*,*,#2501,.T.);
#3599=ORIENTED_EDGE('',*,*,#2502,.T.);
#3600=ORIENTED_EDGE('',*,*,#2501,.F.);
#3601=ORIENTED_EDGE('',*,*,#2500,.T.);
#3602=ORIENTED_EDGE('',*,*,#2499,.T.);
#3603=ORIENTED_EDGE('',*,*,#2502,.F.);
#3604=ORIENTED_EDGE('',*,*,#2490,.T.);
#3750=PLANE('',#4461);
#3751=PLANE('',#4468);
#3752=PLANE('',#4472);
#3753=PLANE('',#4477);
#3754=PLANE('',#4483);
#3755=PLANE('',#4487);
#3756=PLANE('',#4488);
#3976=ADVANCED_FACE('',(#735),#205,.T.);
#3977=ADVANCED_FACE('',(#736),#162,.T.);
#3978=ADVANCED_FACE('',(#737),#3750,.T.);
#3979=ADVANCED_FACE('',(#738),#206,.F.);
#3980=ADVANCED_FACE('',(#739),#163,.T.);
#3981=ADVANCED_FACE('',(#740,#364),#3751,.F.);
#3982=ADVANCED_FACE('',(#741),#164,.T.);
#3983=ADVANCED_FACE('',(#742,#365),#3752,.F.);
#3984=ADVANCED_FACE('',(#743),#165,.T.);
#3985=ADVANCED_FACE('',(#744),#3753,.T.);
#3986=ADVANCED_FACE('',(#745),#166,.T.);
#3987=ADVANCED_FACE('',(#746),#167,.T.);
#3988=ADVANCED_FACE('',(#747,#366),#3754,.T.);
#3989=ADVANCED_FACE('',(#748),#168,.T.);
#3990=ADVANCED_FACE('',(#749,#367),#3755,.T.);
#3991=ADVANCED_FACE('',(#750,#368),#3756,.F.);
#4009=CLOSED_SHELL('',(#3976,#3977,#3978,#3979,#3980,#3981,#3982,#3983,
#3984,#3985,#3986,#3987,#3988,#3989,#3990,#3991));
#4452=AXIS2_PLACEMENT_3D('',#8298,#5453,#5454);
#4453=AXIS2_PLACEMENT_3D('',#8299,#5455,#5456);
#4454=AXIS2_PLACEMENT_3D('',#8301,#5457,#5458);
#4455=AXIS2_PLACEMENT_3D('',#8303,#5459,#5460);
#4456=AXIS2_PLACEMENT_3D('',#8305,#5461,#5462);
#4457=AXIS2_PLACEMENT_3D('',#8306,#5463,#5464);
#4458=AXIS2_PLACEMENT_3D('',#8307,#5465,#5466);
#4459=AXIS2_PLACEMENT_3D('',#8311,#5468,#5469);
#4460=AXIS2_PLACEMENT_3D('',#8312,#5470,#5471);
#4461=AXIS2_PLACEMENT_3D('',#8313,#5472,#5473);
#4462=AXIS2_PLACEMENT_3D('',#8314,#5474,#5475);
#4463=AXIS2_PLACEMENT_3D('',#8317,#5476,#5477);
#4464=AXIS2_PLACEMENT_3D('',#8318,#5478,#5479);
#4465=AXIS2_PLACEMENT_3D('',#8319,#5480,#5481);
#4466=AXIS2_PLACEMENT_3D('',#8320,#5482,#5483);
#4467=AXIS2_PLACEMENT_3D('',#8323,#5485,#5486);
#4468=AXIS2_PLACEMENT_3D('',#8324,#5487,#5488);
#4469=AXIS2_PLACEMENT_3D('',#8326,#5489,#5490);
#4470=AXIS2_PLACEMENT_3D('',#8327,#5491,#5492);
#4471=AXIS2_PLACEMENT_3D('',#8330,#5494,#5495);
#4472=AXIS2_PLACEMENT_3D('',#8331,#5496,#5497);
#4473=AXIS2_PLACEMENT_3D('',#8333,#5498,#5499);
#4474=AXIS2_PLACEMENT_3D('',#8335,#5500,#5501);
#4475=AXIS2_PLACEMENT_3D('',#8336,#5502,#5503);
#4476=AXIS2_PLACEMENT_3D('',#8338,#5504,#5505);
#4477=AXIS2_PLACEMENT_3D('',#8340,#5507,#5508);
#4478=AXIS2_PLACEMENT_3D('',#8341,#5509,#5510);
#4479=AXIS2_PLACEMENT_3D('',#8344,#5512,#5513);
#4480=AXIS2_PLACEMENT_3D('',#8345,#5514,#5515);
#4481=AXIS2_PLACEMENT_3D('',#8347,#5516,#5517);
#4482=AXIS2_PLACEMENT_3D('',#8350,#5519,#5520);
#4483=AXIS2_PLACEMENT_3D('',#8351,#5521,#5522);
#4484=AXIS2_PLACEMENT_3D('',#8352,#5523,#5524);
#4485=AXIS2_PLACEMENT_3D('',#8354,#5525,#5526);
#4486=AXIS2_PLACEMENT_3D('',#8357,#5528,#5529);
#4487=AXIS2_PLACEMENT_3D('',#8358,#5530,#5531);
#4488=AXIS2_PLACEMENT_3D('',#8359,#5532,#5533);
#5453=DIRECTION('axis',(0.,0.,1.));
#5454=DIRECTION('refdir',(1.,0.,0.));
#5455=DIRECTION('center_axis',(-1.,0.,0.));
#5456=DIRECTION('ref_axis',(0.,0.,1.));
#5457=DIRECTION('center_axis',(1.,0.,0.));
#5458=DIRECTION('ref_axis',(0.,-1.,0.));
#5459=DIRECTION('center_axis',(0.,-1.,1.22464679914735E-16));
#5460=DIRECTION('ref_axis',(0.,-1.22464679914735E-16,-1.));
#5461=DIRECTION('center_axis',(-1.,0.,0.));
#5462=DIRECTION('ref_axis',(0.,-1.,0.));
#5463=DIRECTION('center_axis',(-1.,0.,0.));
#5464=DIRECTION('ref_axis',(0.,-1.,0.));
#5465=DIRECTION('center_axis',(-1.,0.,0.));
#5466=DIRECTION('ref_axis',(0.,-1.,0.));
#5467=DIRECTION('',(1.,0.,0.));
#5468=DIRECTION('center_axis',(-1.,0.,0.));
#5469=DIRECTION('ref_axis',(0.,-1.,0.));
#5470=DIRECTION('center_axis',(-1.,0.,0.));
#5471=DIRECTION('ref_axis',(0.,-1.,0.));
#5472=DIRECTION('center_axis',(-1.,0.,0.));
#5473=DIRECTION('ref_axis',(0.,-1.,0.));
#5474=DIRECTION('center_axis',(1.,0.,0.));
#5475=DIRECTION('ref_axis',(0.,0.,-1.));
#5476=DIRECTION('center_axis',(1.,0.,0.));
#5477=DIRECTION('ref_axis',(0.,-1.,0.));
#5478=DIRECTION('center_axis',(1.,0.,0.));
#5479=DIRECTION('ref_axis',(0.,-1.,0.));
#5480=DIRECTION('center_axis',(0.,1.,1.22464679914735E-16));
#5481=DIRECTION('ref_axis',(0.,-1.22464679914735E-16,1.));
#5482=DIRECTION('center_axis',(-1.,0.,0.));
#5483=DIRECTION('ref_axis',(0.,-1.,0.));
#5484=DIRECTION('',(1.,0.,0.));
#5485=DIRECTION('center_axis',(-1.,0.,0.));
#5486=DIRECTION('ref_axis',(0.,-1.,0.));
#5487=DIRECTION('center_axis',(-1.,0.,0.));
#5488=DIRECTION('ref_axis',(0.,-1.,0.));
#5489=DIRECTION('center_axis',(-1.,0.,0.));
#5490=DIRECTION('ref_axis',(0.,-1.,0.));
#5491=DIRECTION('center_axis',(-1.,0.,0.));
#5492=DIRECTION('ref_axis',(0.,-1.,0.));
#5493=DIRECTION('',(1.,0.,0.));
#5494=DIRECTION('center_axis',(1.,0.,0.));
#5495=DIRECTION('ref_axis',(0.,-1.,0.));
#5496=DIRECTION('center_axis',(1.,0.,0.));
#5497=DIRECTION('ref_axis',(0.,1.,0.));
#5498=DIRECTION('center_axis',(1.,0.,0.));
#5499=DIRECTION('ref_axis',(0.,1.,0.));
#5500=DIRECTION('center_axis',(1.,0.,0.));
#5501=DIRECTION('ref_axis',(0.,1.,0.));
#5502=DIRECTION('center_axis',(1.,0.,0.));
#5503=DIRECTION('ref_axis',(0.,1.,0.));
#5504=DIRECTION('center_axis',(1.,0.,0.));
#5505=DIRECTION('ref_axis',(0.,1.,0.));
#5506=DIRECTION('',(-1.,0.,0.));
#5507=DIRECTION('center_axis',(1.,0.,0.));
#5508=DIRECTION('ref_axis',(0.,1.,0.));
#5509=DIRECTION('center_axis',(1.,0.,0.));
#5510=DIRECTION('ref_axis',(0.,1.,0.));
#5511=DIRECTION('',(-1.,0.,0.));
#5512=DIRECTION('center_axis',(-1.,0.,0.));
#5513=DIRECTION('ref_axis',(0.,1.,0.));
#5514=DIRECTION('center_axis',(1.,0.,0.));
#5515=DIRECTION('ref_axis',(0.,1.,0.));
#5516=DIRECTION('center_axis',(1.,0.,0.));
#5517=DIRECTION('ref_axis',(0.,1.,0.));
#5518=DIRECTION('',(-1.,0.,0.));
#5519=DIRECTION('center_axis',(-1.,0.,0.));
#5520=DIRECTION('ref_axis',(0.,1.,0.));
#5521=DIRECTION('center_axis',(1.,0.,0.));
#5522=DIRECTION('ref_axis',(0.,1.,0.));
#5523=DIRECTION('center_axis',(1.,0.,0.));
#5524=DIRECTION('ref_axis',(0.,1.,0.));
#5525=DIRECTION('center_axis',(1.,0.,0.));
#5526=DIRECTION('ref_axis',(0.,1.,0.));
#5527=DIRECTION('',(-1.,0.,0.));
#5528=DIRECTION('center_axis',(1.,0.,0.));
#5529=DIRECTION('ref_axis',(0.,1.,0.));
#5530=DIRECTION('center_axis',(1.,0.,0.));
#5531=DIRECTION('ref_axis',(0.,1.,0.));
#5532=DIRECTION('center_axis',(1.,0.,0.));
#5533=DIRECTION('ref_axis',(0.,1.,0.));
#8298=CARTESIAN_POINT('',(0.,0.,0.));
#8299=CARTESIAN_POINT('Origin',(-25.,0.,0.));
#8300=CARTESIAN_POINT('',(-26.5,-9.79717439317883E-16,-8.));
#8301=CARTESIAN_POINT('Origin',(-26.5,0.,0.));
#8302=CARTESIAN_POINT('',(-25.,-1.16341445918999E-15,-9.5));
#8303=CARTESIAN_POINT('Origin',(-25.,-9.79717439317883E-16,-8.));
#8304=CARTESIAN_POINT('',(-25.,9.5,-1.16341445918999E-15));
#8305=CARTESIAN_POINT('Origin',(-25.,0.,0.));
#8306=CARTESIAN_POINT('Origin',(-25.,0.,0.));
#8307=CARTESIAN_POINT('Origin',(-6.5,0.,0.));
#8308=CARTESIAN_POINT('',(-19.7496152242889,9.5,-1.16341445918999E-15));
#8309=CARTESIAN_POINT('',(-6.5,9.5,-1.16341445918999E-15));
#8310=CARTESIAN_POINT('',(-19.7496152242889,-1.16341445918999E-15,9.5));
#8311=CARTESIAN_POINT('Origin',(-19.7496152242889,0.,0.));
#8312=CARTESIAN_POINT('Origin',(-19.7496152242889,0.,0.));
#8313=CARTESIAN_POINT('Origin',(-26.5,0.,0.));
#8314=CARTESIAN_POINT('Origin',(-16.5,0.,0.));
#8315=CARTESIAN_POINT('',(-13.2503847757111,9.5,1.16341445918999E-15));
#8316=CARTESIAN_POINT('',(-13.2503847757111,-1.16341445918999E-15,9.5));
#8317=CARTESIAN_POINT('Origin',(-13.2503847757111,0.,0.));
#8318=CARTESIAN_POINT('Origin',(-13.2503847757111,0.,0.));
#8319=CARTESIAN_POINT('Origin',(-16.5,-1.46957618087521E-15,12.0000001788139));
#8320=CARTESIAN_POINT('Origin',(-6.5,0.,0.));
#8321=CARTESIAN_POINT('',(-6.5,9.5,-1.16341445918999E-15));
#8322=CARTESIAN_POINT('',(-6.5,9.5,-1.16341445918999E-15));
#8323=CARTESIAN_POINT('Origin',(-6.5,0.,0.));
#8324=CARTESIAN_POINT('Origin',(-6.5,0.,0.));
#8325=CARTESIAN_POINT('',(-6.5,6.5,-7.96020419445779E-16));
#8326=CARTESIAN_POINT('Origin',(-6.5,0.,0.));
#8327=CARTESIAN_POINT('Origin',(0.,0.,0.));
#8328=CARTESIAN_POINT('',(0.,6.5,-7.96020419445779E-16));
#8329=CARTESIAN_POINT('',(0.,6.5,-7.96020419445779E-16));
#8330=CARTESIAN_POINT('Origin',(0.,0.,0.));
#8331=CARTESIAN_POINT('Origin',(113.5,0.,0.));
#8332=CARTESIAN_POINT('',(113.5,-6.50000009685755,-7.96020431307408E-16));
#8333=CARTESIAN_POINT('Origin',(113.5,0.,0.));
#8334=CARTESIAN_POINT('',(113.5,-4.75,-5.81707229594993E-16));
#8335=CARTESIAN_POINT('Origin',(113.5,0.,0.));
#8336=CARTESIAN_POINT('Origin',(113.5,0.,0.));
#8337=CARTESIAN_POINT('',(133.5,-6.50000009685755,-7.96020431307408E-16));
#8338=CARTESIAN_POINT('Origin',(133.5,0.,0.));
#8339=CARTESIAN_POINT('',(113.5,-6.50000009685755,-7.96020431307408E-16));
#8340=CARTESIAN_POINT('Origin',(133.5,0.,0.));
#8341=CARTESIAN_POINT('Origin',(110.,0.,0.));
#8342=CARTESIAN_POINT('',(110.,-4.75,-5.81707229594993E-16));
#8343=CARTESIAN_POINT('',(110.,-4.75,-5.81707229594993E-16));
#8344=CARTESIAN_POINT('Origin',(110.,0.,0.));
#8345=CARTESIAN_POINT('Origin',(100.5,0.,0.));
#8346=CARTESIAN_POINT('',(110.,-6.5,-7.9602041944578E-16));
#8347=CARTESIAN_POINT('Origin',(110.,0.,0.));
#8348=CARTESIAN_POINT('',(100.5,-6.5,-7.9602041944578E-16));
#8349=CARTESIAN_POINT('',(100.5,-6.5,-7.9602041944578E-16));
#8350=CARTESIAN_POINT('Origin',(100.5,0.,0.));
#8351=CARTESIAN_POINT('Origin',(110.,0.,0.));
#8352=CARTESIAN_POINT('Origin',(0.,0.,0.));
#8353=CARTESIAN_POINT('',(100.5,-8.,-9.79717439317883E-16));
#8354=CARTESIAN_POINT('Origin',(100.5,0.,0.));
#8355=CARTESIAN_POINT('',(0.,-8.,-9.79717439317883E-16));
#8356=CARTESIAN_POINT('',(0.,-8.,-9.79717439317883E-16));
#8357=CARTESIAN_POINT('Origin',(0.,0.,0.));
#8358=CARTESIAN_POINT('Origin',(100.5,0.,0.));
#8359=CARTESIAN_POINT('Origin',(0.,0.,0.));
#8432=UNCERTAINTY_MEASURE_WITH_UNIT(LENGTH_MEASURE(0.01),#8446,
'DISTANCE_ACCURACY_VALUE',
'Maximum model space distance between geometric entities at asserted c
onnectivities');
#8434=UNCERTAINTY_MEASURE_WITH_UNIT(LENGTH_MEASURE(0.01),#8446,
'DISTANCE_ACCURACY_VALUE',
'Maximum model space distance between geometric entities at asserted c
onnectivities');
#8443=(
GEOMETRIC_REPRESENTATION_CONTEXT(3)
GLOBAL_UNCERTAINTY_ASSIGNED_CONTEXT((#8432))
GLOBAL_UNIT_ASSIGNED_CONTEXT((#8446,#8448,#8449))
REPRESENTATION_CONTEXT('','3D')
);
#8445=(
GEOMETRIC_REPRESENTATION_CONTEXT(3)
GLOBAL_UNCERTAINTY_ASSIGNED_CONTEXT((#8434))
GLOBAL_UNIT_ASSIGNED_CONTEXT((#8446,#8448,#8449))
REPRESENTATION_CONTEXT('','3D')
);
#8446=(
LENGTH_UNIT()
NAMED_UNIT(*)
SI_UNIT(.MILLI.,.METRE.)
);
#8448=(
NAMED_UNIT(*)
PLANE_ANGLE_UNIT()
SI_UNIT($,.RADIAN.)
);
#8449=(
NAMED_UNIT(*)
SI_UNIT($,.STERADIAN.)
SOLID_ANGLE_UNIT()
);
#8458=SHAPE_DEFINITION_REPRESENTATION(#8468,#8491);
#8468=PRODUCT_DEFINITION_SHAPE('',$,#8502);
#8491=SHAPE_REPRESENTATION('',(#4452),#8443);
#8493=PRODUCT_DEFINITION_CONTEXT('part definition',#8525,'design');
#8502=PRODUCT_DEFINITION('2026-10-05-11-51-15-581','PO4',#8512,#8493);
#8512=PRODUCT_DEFINITION_FORMATION('',$,#8535);
#8525=APPLICATION_CONTEXT(
'Core Data for Automotive Mechanical Design Process');
#8526=PRODUCT_CONTEXT('part definition',#8525,'mechanical');
#8535=PRODUCT('2026-10-05-11-51-15-581','PO4',$,(#8526));
#8537=PRESENTATION_STYLE_ASSIGNMENT((#8538));
#8538=SURFACE_STYLE_USAGE(.BOTH.,#8539);
#8539=SURFACE_SIDE_STYLE('',(#8540));
#8540=SURFACE_STYLE_FILL_AREA(#8541);
#8541=FILL_AREA_STYLE('Steel - Satin',(#8542));
#8542=FILL_AREA_STYLE_COLOUR('Steel - Satin',#8543);
#8543=COLOUR_RGB('Steel - Satin', 0.09019608, 0.27058824, 0.51372549);
ENDSEC;
END-ISO-10303-21;
